ISO-10303-21;
HEADER;
/* Generated by software containing ST-Developer
 * from STEP Tools, Inc. (www.steptools.com) 
 */

FILE_DESCRIPTION(
/* description */ ('PAT-082'),
/* implementation_level */ '2;1');

FILE_NAME(
/* name */ 'Body.step',
/* time_stamp */ '2026-10-29T20:16:13-07:00',
/* author */ (''),
/* organization */ (''),
/* preprocessor_version */ 'ST-DEVELOPER v20.2',
/* originating_system */ 'Autodesk Translation Framework v15.17.0.0',
/* authorisation */ '');

FILE_SCHEMA (('AUTOMOTIVE_DESIGN { 1 0 10303 214 3 1 1 }'));
ENDSEC;

DATA;
#10=MECHANICAL_DESIGN_GEOMETRIC_PRESENTATION_REPRESENTATION('',(#258),#8266);
#214=SHAPE_REPRESENTATION_RELATIONSHIP('SRR','None',#8377,#236);
#236=ADVANCED_BREP_SHAPE_REPRESENTATION('',(#279),#8261);
#258=STYLED_ITEM('',(#8516),#279);
#279=MANIFOLD_SOLID_BREP('Body1',#4599);
#390=FACE_BOUND('',#1151,.T.);
#391=FACE_BOUND('',#1153,.T.);
#392=FACE_BOUND('',#1155,.T.);
#393=FACE_BOUND('',#1163,.T.);
#394=FACE_BOUND('',#1166,.T.);
#395=FACE_BOUND('',#1170,.T.);
#525=PLANE('',#5232);
#526=PLANE('',#5234);
#527=PLANE('',#5236);
#528=PLANE('',#5238);
#529=PLANE('',#5239);
#530=PLANE('',#5240);
#531=PLANE('',#5241);
#532=PLANE('',#5242);
#533=PLANE('',#5243);
#534=PLANE('',#5244);
#535=PLANE('',#5248);
#536=PLANE('',#5253);
#771=FACE_OUTER_BOUND('',#1149,.T.);
#772=FACE_OUTER_BOUND('',#1150,.T.);
#773=FACE_OUTER_BOUND('',#1152,.T.);
#774=FACE_OUTER_BOUND('',#1154,.T.);
#775=FACE_OUTER_BOUND('',#1156,.T.);
#776=FACE_OUTER_BOUND('',#1157,.T.);
#777=FACE_OUTER_BOUND('',#1158,.T.);
#778=FACE_OUTER_BOUND('',#1159,.T.);
#779=FACE_OUTER_BOUND('',#1160,.T.);
#780=FACE_OUTER_BOUND('',#1161,.T.);
#781=FACE_OUTER_BOUND('',#1162,.T.);
#782=FACE_OUTER_BOUND('',#1164,.T.);
#783=FACE_OUTER_BOUND('',#1165,.T.);
#784=FACE_OUTER_BOUND('',#1167,.T.);
#785=FACE_OUTER_BOUND('',#1168,.T.);
#786=FACE_OUTER_BOUND('',#1169,.T.);
#787=FACE_OUTER_BOUND('',#1171,.T.);
#1149=EDGE_LOOP('',(#3950,#3951,#3952,#3953));
#1150=EDGE_LOOP('',(#3954));
#1151=EDGE_LOOP('',(#3955));
#1152=EDGE_LOOP('',(#3956,#3957,#3958,#3959,#3960,#3961));
#1153=EDGE_LOOP('',(#3962));
#1154=EDGE_LOOP('',(#3963,#3964,#3965,#3966,#3967,#3968));
#1155=EDGE_LOOP('',(#3969));
#1156=EDGE_LOOP('',(#3970,#3971,#3972,#3973));
#1157=EDGE_LOOP('',(#3974,#3975,#3976,#3977));
#1158=EDGE_LOOP('',(#3978,#3979,#3980,#3981));
#1159=EDGE_LOOP('',(#3982,#3983,#3984,#3985));
#1160=EDGE_LOOP('',(#3986,#3987,#3988,#3989));
#1161=EDGE_LOOP('',(#3990,#3991,#3992,#3993));
#1162=EDGE_LOOP('',(#3994));
#1163=EDGE_LOOP('',(#3995));
#1164=EDGE_LOOP('',(#3996,#3997,#3998,#3999));
#1165=EDGE_LOOP('',(#4000));
#1166=EDGE_LOOP('',(#4001));
#1167=EDGE_LOOP('',(#4002,#4003,#4004,#4005));
#1168=EDGE_LOOP('',(#4006,#4007,#4008,#4009));
#1169=EDGE_LOOP('',(#4010));
#1170=EDGE_LOOP('',(#4011));
#1171=EDGE_LOOP('',(#4012,#4013,#4014,#4015));
#1494=LINE('',#7885,#1849);
#1495=LINE('',#7893,#1850);
#1496=LINE('',#7895,#1851);
#1497=LINE('',#7897,#1852);
#1498=LINE('',#7899,#1853);
#1499=LINE('',#7901,#1854);
#1500=LINE('',#7902,#1855);
#1501=LINE('',#7908,#1856);
#1502=LINE('',#7910,#1857);
#1503=LINE('',#7912,#1858);
#1504=LINE('',#7914,#1859);
#1505=LINE('',#7916,#1860);
#1506=LINE('',#7917,#1861);
#1507=LINE('',#7921,#1862);
#1508=LINE('',#7922,#1863);
#1509=LINE('',#7924,#1864);
#1510=LINE('',#7926,#1865);
#1511=LINE('',#7928,#1866);
#1512=LINE('',#7930,#1867);
#1513=LINE('',#7937,#1868);
#1514=LINE('',#7943,#1869);
#1515=LINE('',#7947,#1870);
#1516=LINE('',#7952,#1871);
#1849=VECTOR('',#6405,0.43);
#1850=VECTOR('',#6414,1.);
#1851=VECTOR('',#6415,1.);
#1852=VECTOR('',#6416,1.);
#1853=VECTOR('',#6417,1.);
#1854=VECTOR('',#6418,1.);
#1855=VECTOR('',#6419,1.);
#1856=VECTOR('',#6424,1.);
#1857=VECTOR('',#6425,1.);
#1858=VECTOR('',#6426,1.);
#1859=VECTOR('',#6427,1.);
#1860=VECTOR('',#6428,1.);
#1861=VECTOR('',#6429,1.);
#1862=VECTOR('',#6434,1.);
#1863=VECTOR('',#6435,1.);
#1864=VECTOR('',#6438,1.);
#1865=VECTOR('',#6441,1.);
#1866=VECTOR('',#6444,1.);
#1867=VECTOR('',#6447,1.);
#1868=VECTOR('',#6456,0.46);
#1869=VECTOR('',#6465,0.525);
#1870=VECTOR('',#6470,0.515);
#1871=VECTOR('',#6477,0.2);
#2106=CIRCLE('',#5230,0.43);
#2107=CIRCLE('',#5231,0.43);
#2108=CIRCLE('',#5233,0.2);
#2109=CIRCLE('',#5235,0.525);
#2110=CIRCLE('',#5237,0.515);
#2111=CIRCLE('',#5245,0.46);
#2112=CIRCLE('',#5247,0.46);
#2113=CIRCLE('',#5249,0.525);
#2114=CIRCLE('',#5252,0.515);
#2115=CIRCLE('',#5254,0.2);
#2432=VERTEX_POINT('',#7882);
#2433=VERTEX_POINT('',#7884);
#2434=VERTEX_POINT('',#7888);
#2435=VERTEX_POINT('',#7891);
#2436=VERTEX_POINT('',#7892);
#2437=VERTEX_POINT('',#7894);
#2438=VERTEX_POINT('',#7896);
#2439=VERTEX_POINT('',#7898);
#2440=VERTEX_POINT('',#7900);
#2441=VERTEX_POINT('',#7903);
#2442=VERTEX_POINT('',#7906);
#2443=VERTEX_POINT('',#7907);
#2444=VERTEX_POINT('',#7909);
#2445=VERTEX_POINT('',#7911);
#2446=VERTEX_POINT('',#7913);
#2447=VERTEX_POINT('',#7915);
#2448=VERTEX_POINT('',#7918);
#2449=VERTEX_POINT('',#7933);
#2450=VERTEX_POINT('',#7936);
#2451=VERTEX_POINT('',#7940);
#2452=VERTEX_POINT('',#7945);
#2453=VERTEX_POINT('',#7949);
#2951=EDGE_CURVE('',#2432,#2432,#2106,.T.);
#2952=EDGE_CURVE('',#2432,#2433,#1494,.T.);
#2953=EDGE_CURVE('',#2433,#2433,#2107,.T.);
#2954=EDGE_CURVE('',#2434,#2434,#2108,.T.);
#2955=EDGE_CURVE('',#2435,#2436,#1495,.T.);
#2956=EDGE_CURVE('',#2436,#2437,#1496,.T.);
#2957=EDGE_CURVE('',#2437,#2438,#1497,.T.);
#2958=EDGE_CURVE('',#2438,#2439,#1498,.T.);
#2959=EDGE_CURVE('',#2439,#2440,#1499,.T.);
#2960=EDGE_CURVE('',#2440,#2435,#1500,.T.);
#2961=EDGE_CURVE('',#2441,#2441,#2109,.T.);
#2962=EDGE_CURVE('',#2442,#2443,#1501,.T.);
#2963=EDGE_CURVE('',#2444,#2442,#1502,.T.);
#2964=EDGE_CURVE('',#2445,#2444,#1503,.T.);
#2965=EDGE_CURVE('',#2446,#2445,#1504,.T.);
#2966=EDGE_CURVE('',#2447,#2446,#1505,.T.);
#2967=EDGE_CURVE('',#2443,#2447,#1506,.T.);
#2968=EDGE_CURVE('',#2448,#2448,#2110,.T.);
#2969=EDGE_CURVE('',#2442,#2435,#1507,.T.);
#2970=EDGE_CURVE('',#2444,#2440,#1508,.T.);
#2971=EDGE_CURVE('',#2445,#2439,#1509,.T.);
#2972=EDGE_CURVE('',#2446,#2438,#1510,.T.);
#2973=EDGE_CURVE('',#2447,#2437,#1511,.T.);
#2974=EDGE_CURVE('',#2443,#2436,#1512,.T.);
#2975=EDGE_CURVE('',#2449,#2449,#2111,.T.);
#2976=EDGE_CURVE('',#2449,#2450,#1513,.T.);
#2977=EDGE_CURVE('',#2450,#2450,#2112,.T.);
#2978=EDGE_CURVE('',#2451,#2451,#2113,.T.);
#2979=EDGE_CURVE('',#2441,#2451,#1514,.T.);
#2980=EDGE_CURVE('',#2452,#2452,#2114,.T.);
#2981=EDGE_CURVE('',#2452,#2448,#1515,.T.);
#2982=EDGE_CURVE('',#2453,#2453,#2115,.T.);
#2983=EDGE_CURVE('',#2453,#2434,#1516,.T.);
#3950=ORIENTED_EDGE('',*,*,#2951,.F.);
#3951=ORIENTED_EDGE('',*,*,#2952,.T.);
#3952=ORIENTED_EDGE('',*,*,#2953,.F.);
#3953=ORIENTED_EDGE('',*,*,#2952,.F.);
#3954=ORIENTED_EDGE('',*,*,#2951,.T.);
#3955=ORIENTED_EDGE('',*,*,#2954,.F.);
#3956=ORIENTED_EDGE('',*,*,#2955,.T.);
#3957=ORIENTED_EDGE('',*,*,#2956,.T.);
#3958=ORIENTED_EDGE('',*,*,#2957,.T.);
#3959=ORIENTED_EDGE('',*,*,#2958,.T.);
#3960=ORIENTED_EDGE('',*,*,#2959,.T.);
#3961=ORIENTED_EDGE('',*,*,#2960,.T.);
#3962=ORIENTED_EDGE('',*,*,#2961,.T.);
#3963=ORIENTED_EDGE('',*,*,#2962,.F.);
#3964=ORIENTED_EDGE('',*,*,#2963,.F.);
#3965=ORIENTED_EDGE('',*,*,#2964,.F.);
#3966=ORIENTED_EDGE('',*,*,#2965,.F.);
#3967=ORIENTED_EDGE('',*,*,#2966,.F.);
#3968=ORIENTED_EDGE('',*,*,#2967,.F.);
#3969=ORIENTED_EDGE('',*,*,#2968,.F.);
#3970=ORIENTED_EDGE('',*,*,#2963,.T.);
#3971=ORIENTED_EDGE('',*,*,#2969,.T.);
#3972=ORIENTED_EDGE('',*,*,#2960,.F.);
#3973=ORIENTED_EDGE('',*,*,#2970,.F.);
#3974=ORIENTED_EDGE('',*,*,#2964,.T.);
#3975=ORIENTED_EDGE('',*,*,#2970,.T.);
#3976=ORIENTED_EDGE('',*,*,#2959,.F.);
#3977=ORIENTED_EDGE('',*,*,#2971,.F.);
#3978=ORIENTED_EDGE('',*,*,#2965,.T.);
#3979=ORIENTED_EDGE('',*,*,#2971,.T.);
#3980=ORIENTED_EDGE('',*,*,#2958,.F.);
#3981=ORIENTED_EDGE('',*,*,#2972,.F.);
#3982=ORIENTED_EDGE('',*,*,#2966,.T.);
#3983=ORIENTED_EDGE('',*,*,#2972,.T.);
#3984=ORIENTED_EDGE('',*,*,#2957,.F.);
#3985=ORIENTED_EDGE('',*,*,#2973,.F.);
#3986=ORIENTED_EDGE('',*,*,#2967,.T.);
#3987=ORIENTED_EDGE('',*,*,#2973,.T.);
#3988=ORIENTED_EDGE('',*,*,#2956,.F.);
#3989=ORIENTED_EDGE('',*,*,#2974,.F.);
#3990=ORIENTED_EDGE('',*,*,#2962,.T.);
#3991=ORIENTED_EDGE('',*,*,#2974,.T.);
#3992=ORIENTED_EDGE('',*,*,#2955,.F.);
#3993=ORIENTED_EDGE('',*,*,#2969,.F.);
#3994=ORIENTED_EDGE('',*,*,#2975,.F.);
#3995=ORIENTED_EDGE('',*,*,#2953,.T.);
#3996=ORIENTED_EDGE('',*,*,#2975,.T.);
#3997=ORIENTED_EDGE('',*,*,#2976,.T.);
#3998=ORIENTED_EDGE('',*,*,#2977,.F.);
#3999=ORIENTED_EDGE('',*,*,#2976,.F.);
#4000=ORIENTED_EDGE('',*,*,#2978,.F.);
#4001=ORIENTED_EDGE('',*,*,#2977,.T.);
#4002=ORIENTED_EDGE('',*,*,#2961,.F.);
#4003=ORIENTED_EDGE('',*,*,#2979,.T.);
#4004=ORIENTED_EDGE('',*,*,#2978,.T.);
#4005=ORIENTED_EDGE('',*,*,#2979,.F.);
#4006=ORIENTED_EDGE('',*,*,#2980,.F.);
#4007=ORIENTED_EDGE('',*,*,#2981,.T.);
#4008=ORIENTED_EDGE('',*,*,#2968,.T.);
#4009=ORIENTED_EDGE('',*,*,#2981,.F.);
#4010=ORIENTED_EDGE('',*,*,#2980,.T.);
#4011=ORIENTED_EDGE('',*,*,#2982,.F.);
#4012=ORIENTED_EDGE('',*,*,#2982,.T.);
#4013=ORIENTED_EDGE('',*,*,#2983,.T.);
#4014=ORIENTED_EDGE('',*,*,#2954,.T.);
#4015=ORIENTED_EDGE('',*,*,#2983,.F.);
#4296=CYLINDRICAL_SURFACE('',#5229,0.43);
#4297=CYLINDRICAL_SURFACE('',#5246,0.46);
#4298=CYLINDRICAL_SURFACE('',#5250,0.525);
#4299=CYLINDRICAL_SURFACE('',#5251,0.515);
#4300=CYLINDRICAL_SURFACE('',#5255,0.2);
#4510=ADVANCED_FACE('',(#771),#4296,.F.);
#4511=ADVANCED_FACE('',(#772,#390),#525,.T.);
#4512=ADVANCED_FACE('',(#773,#391),#526,.T.);
#4513=ADVANCED_FACE('',(#774,#392),#527,.F.);
#4514=ADVANCED_FACE('',(#775),#528,.T.);
#4515=ADVANCED_FACE('',(#776),#529,.T.);
#4516=ADVANCED_FACE('',(#777),#530,.T.);
#4517=ADVANCED_FACE('',(#778),#531,.T.);
#4518=ADVANCED_FACE('',(#779),#532,.T.);
#4519=ADVANCED_FACE('',(#780),#533,.T.);
#4520=ADVANCED_FACE('',(#781,#393),#534,.T.);
#4521=ADVANCED_FACE('',(#782),#4297,.F.);
#4522=ADVANCED_FACE('',(#783,#394),#535,.T.);
#4523=ADVANCED_FACE('',(#784),#4298,.T.);
#4524=ADVANCED_FACE('',(#785),#4299,.T.);
#4525=ADVANCED_FACE('',(#786,#395),#536,.T.);
#4526=ADVANCED_FACE('',(#787),#4300,.F.);
#4599=CLOSED_SHELL('',(#4510,#4511,#4512,#4513,#4514,#4515,#4516,#4517,
#4518,#4519,#4520,#4521,#4522,#4523,#4524,#4525,#4526));
#5228=AXIS2_PLACEMENT_3D('',#7880,#6399,#6400);
#5229=AXIS2_PLACEMENT_3D('',#7881,#6401,#6402);
#5230=AXIS2_PLACEMENT_3D('',#7883,#6403,#6404);
#5231=AXIS2_PLACEMENT_3D('',#7886,#6406,#6407);
#5232=AXIS2_PLACEMENT_3D('',#7887,#6408,#6409);
#5233=AXIS2_PLACEMENT_3D('',#7889,#6410,#6411);
#5234=AXIS2_PLACEMENT_3D('',#7890,#6412,#6413);
#5235=AXIS2_PLACEMENT_3D('',#7904,#6420,#6421);
#5236=AXIS2_PLACEMENT_3D('',#7905,#6422,#6423);
#5237=AXIS2_PLACEMENT_3D('',#7919,#6430,#6431);
#5238=AXIS2_PLACEMENT_3D('',#7920,#6432,#6433);
#5239=AXIS2_PLACEMENT_3D('',#7923,#6436,#6437);
#5240=AXIS2_PLACEMENT_3D('',#7925,#6439,#6440);
#5241=AXIS2_PLACEMENT_3D('',#7927,#6442,#6443);
#5242=AXIS2_PLACEMENT_3D('',#7929,#6445,#6446);
#5243=AXIS2_PLACEMENT_3D('',#7931,#6448,#6449);
#5244=AXIS2_PLACEMENT_3D('',#7932,#6450,#6451);
#5245=AXIS2_PLACEMENT_3D('',#7934,#6452,#6453);
#5246=AXIS2_PLACEMENT_3D('',#7935,#6454,#6455);
#5247=AXIS2_PLACEMENT_3D('',#7938,#6457,#6458);
#5248=AXIS2_PLACEMENT_3D('',#7939,#6459,#6460);
#5249=AXIS2_PLACEMENT_3D('',#7941,#6461,#6462);
#5250=AXIS2_PLACEMENT_3D('',#7942,#6463,#6464);
#5251=AXIS2_PLACEMENT_3D('',#7944,#6466,#6467);
#5252=AXIS2_PLACEMENT_3D('',#7946,#6468,#6469);
#5253=AXIS2_PLACEMENT_3D('',#7948,#6471,#6472);
#5254=AXIS2_PLACEMENT_3D('',#7950,#6473,#6474);
#5255=AXIS2_PLACEMENT_3D('',#7951,#6475,#6476);
#6399=DIRECTION('axis',(0.,0.,1.));
#6400=DIRECTION('refdir',(1.,0.,0.));
#6401=DIRECTION('center_axis',(0.,1.,0.));
#6402=DIRECTION('ref_axis',(1.,0.,0.));
#6403=DIRECTION('center_axis',(0.,1.,0.));
#6404=DIRECTION('ref_axis',(1.,0.,0.));
#6405=DIRECTION('',(0.,1.,0.));
#6406=DIRECTION('center_axis',(0.,-1.,0.));
#6407=DIRECTION('ref_axis',(1.,0.,0.));
#6408=DIRECTION('center_axis',(0.,1.,0.));
#6409=DIRECTION('ref_axis',(1.,0.,0.));
#6410=DIRECTION('center_axis',(0.,1.,0.));
#6411=DIRECTION('ref_axis',(1.,0.,0.));
#6412=DIRECTION('center_axis',(0.,1.,0.));
#6413=DIRECTION('ref_axis',(1.,0.,0.));
#6414=DIRECTION('',(0.5,0.,-0.866025403784439));
#6415=DIRECTION('',(-0.5,0.,-0.866025403784439));
#6416=DIRECTION('',(-1.,0.,-1.60246890531964E-16));
#6417=DIRECTION('',(-0.5,0.,0.866025403784439));
#6418=DIRECTION('',(0.5,0.,0.866025403784439));
#6419=DIRECTION('',(1.,0.,1.60246890531964E-16));
#6420=DIRECTION('center_axis',(0.,-1.,0.));
#6421=DIRECTION('ref_axis',(1.,0.,0.));
#6422=DIRECTION('center_axis',(0.,1.,0.));
#6423=DIRECTION('ref_axis',(1.,0.,0.));
#6424=DIRECTION('',(0.5,0.,-0.866025403784439));
#6425=DIRECTION('',(1.,0.,1.60246890531964E-16));
#6426=DIRECTION('',(0.5,0.,0.866025403784439));
#6427=DIRECTION('',(-0.5,0.,0.866025403784439));
#6428=DIRECTION('',(-1.,0.,-1.60246890531964E-16));
#6429=DIRECTION('',(-0.5,0.,-0.866025403784439));
#6430=DIRECTION('center_axis',(0.,-1.,0.));
#6431=DIRECTION('ref_axis',(1.,0.,0.));
#6432=DIRECTION('center_axis',(-1.60246890531964E-16,0.,1.));
#6433=DIRECTION('ref_axis',(1.,0.,1.60246890531964E-16));
#6434=DIRECTION('',(0.,1.,0.));
#6435=DIRECTION('',(0.,1.,0.));
#6436=DIRECTION('center_axis',(-0.866025403784439,0.,0.5));
#6437=DIRECTION('ref_axis',(0.5,0.,0.866025403784439));
#6438=DIRECTION('',(0.,1.,0.));
#6439=DIRECTION('center_axis',(-0.866025403784439,0.,-0.5));
#6440=DIRECTION('ref_axis',(-0.5,0.,0.866025403784439));
#6441=DIRECTION('',(0.,1.,0.));
#6442=DIRECTION('center_axis',(1.60246890531964E-16,0.,-1.));
#6443=DIRECTION('ref_axis',(-1.,0.,-1.60246890531964E-16));
#6444=DIRECTION('',(0.,1.,0.));
#6445=DIRECTION('center_axis',(0.866025403784439,0.,-0.5));
#6446=DIRECTION('ref_axis',(-0.5,0.,-0.866025403784439));
#6447=DIRECTION('',(0.,1.,0.));
#6448=DIRECTION('center_axis',(0.866025403784439,0.,0.5));
#6449=DIRECTION('ref_axis',(0.5,0.,-0.866025403784439));
#6450=DIRECTION('center_axis',(0.,1.,0.));
#6451=DIRECTION('ref_axis',(0.,0.,1.));
#6452=DIRECTION('center_axis',(0.,-1.,0.));
#6453=DIRECTION('ref_axis',(1.,0.,0.));
#6454=DIRECTION('center_axis',(0.,-1.,0.));
#6455=DIRECTION('ref_axis',(1.,0.,0.));
#6456=DIRECTION('',(0.,1.,0.));
#6457=DIRECTION('center_axis',(0.,-1.,0.));
#6458=DIRECTION('ref_axis',(1.,0.,0.));
#6459=DIRECTION('center_axis',(0.,1.,0.));
#6460=DIRECTION('ref_axis',(0.,0.,1.));
#6461=DIRECTION('center_axis',(0.,-1.,0.));
#6462=DIRECTION('ref_axis',(1.,0.,0.));
#6463=DIRECTION('center_axis',(0.,-1.,0.));
#6464=DIRECTION('ref_axis',(1.,0.,0.));
#6465=DIRECTION('',(0.,1.,0.));
#6466=DIRECTION('center_axis',(0.,-1.,0.));
#6467=DIRECTION('ref_axis',(1.,0.,0.));
#6468=DIRECTION('center_axis',(0.,-1.,0.));
#6469=DIRECTION('ref_axis',(1.,0.,0.));
#6470=DIRECTION('',(0.,1.,0.));
#6471=DIRECTION('center_axis',(0.,-1.,0.));
#6472=DIRECTION('ref_axis',(0.,0.,-1.));
#6473=DIRECTION('center_axis',(0.,-1.,0.));
#6474=DIRECTION('ref_axis',(1.,0.,0.));
#6475=DIRECTION('center_axis',(0.,-1.,0.));
#6476=DIRECTION('ref_axis',(1.,0.,0.));
#6477=DIRECTION('',(0.,1.,0.));
#7880=CARTESIAN_POINT('',(0.,0.,0.));
#7881=CARTESIAN_POINT('Origin',(0.,0.6,0.));
#7882=CARTESIAN_POINT('',(-0.43,0.6,5.26598123633362E-17));
#7883=CARTESIAN_POINT('Origin',(0.,0.6,0.));
#7884=CARTESIAN_POINT('',(-0.43,0.7,-5.26598123633362E-17));
#7885=CARTESIAN_POINT('',(-0.43,0.6,5.26598123633362E-17));
#7886=CARTESIAN_POINT('Origin',(0.,0.7,0.));
#7887=CARTESIAN_POINT('Origin',(0.,0.6,0.));
#7888=CARTESIAN_POINT('',(-0.2,0.6,2.44929359829471E-17));
#7889=CARTESIAN_POINT('Origin',(0.,0.6,0.));
#7890=CARTESIAN_POINT('Origin',(0.,0.5,-1.11022302462516E-16));
#7891=CARTESIAN_POINT('',(0.346410161513776,0.5,0.6));
#7892=CARTESIAN_POINT('',(0.692820323027551,0.5,0.));
#7893=CARTESIAN_POINT('',(0.346410161513776,0.5,0.6));
#7894=CARTESIAN_POINT('',(0.346410161513776,0.5,-0.6));
#7895=CARTESIAN_POINT('',(0.692820323027551,0.5,0.));
#7896=CARTESIAN_POINT('',(-0.346410161513775,0.5,-0.6));
#7897=CARTESIAN_POINT('',(0.346410161513776,0.5,-0.6));
#7898=CARTESIAN_POINT('',(-0.692820323027551,0.5,-8.48460190979926E-17));
#7899=CARTESIAN_POINT('',(-0.346410161513775,0.5,-0.6));
#7900=CARTESIAN_POINT('',(-0.346410161513776,0.5,0.6));
#7901=CARTESIAN_POINT('',(-0.692820323027551,0.5,-8.48460190979926E-17));
#7902=CARTESIAN_POINT('',(-0.346410161513776,0.5,0.6));
#7903=CARTESIAN_POINT('',(-0.525,0.5,-6.4293956955236E-17));
#7904=CARTESIAN_POINT('Origin',(0.,0.5,0.));
#7905=CARTESIAN_POINT('Origin',(0.,0.,-1.11022302462516E-16));
#7906=CARTESIAN_POINT('',(0.346410161513776,0.,0.6));
#7907=CARTESIAN_POINT('',(0.692820323027551,0.,0.));
#7908=CARTESIAN_POINT('',(0.346410161513776,0.,0.6));
#7909=CARTESIAN_POINT('',(-0.346410161513776,0.,0.6));
#7910=CARTESIAN_POINT('',(-0.346410161513776,0.,0.6));
#7911=CARTESIAN_POINT('',(-0.692820323027551,0.,-8.48460190979926E-17));
#7912=CARTESIAN_POINT('',(-0.692820323027551,0.,-8.48460190979926E-17));
#7913=CARTESIAN_POINT('',(-0.346410161513775,0.,-0.6));
#7914=CARTESIAN_POINT('',(-0.346410161513775,0.,-0.6));
#7915=CARTESIAN_POINT('',(0.346410161513776,0.,-0.6));
#7916=CARTESIAN_POINT('',(0.346410161513776,0.,-0.6));
#7917=CARTESIAN_POINT('',(0.692820323027551,0.,0.));
#7918=CARTESIAN_POINT('',(-0.515,0.,-6.30693101560887E-17));
#7919=CARTESIAN_POINT('Origin',(0.,0.,0.));
#7920=CARTESIAN_POINT('Origin',(-0.346410161513776,0.,0.6));
#7921=CARTESIAN_POINT('',(0.346410161513776,0.,0.6));
#7922=CARTESIAN_POINT('',(-0.346410161513776,0.,0.6));
#7923=CARTESIAN_POINT('Origin',(-0.692820323027551,0.,-8.48460190979926E-17));
#7924=CARTESIAN_POINT('',(-0.692820323027551,0.,-8.48460190979926E-17));
#7925=CARTESIAN_POINT('Origin',(-0.346410161513775,0.,-0.6));
#7926=CARTESIAN_POINT('',(-0.346410161513775,0.,-0.6));
#7927=CARTESIAN_POINT('Origin',(0.346410161513776,0.,-0.6));
#7928=CARTESIAN_POINT('',(0.346410161513776,0.,-0.6));
#7929=CARTESIAN_POINT('Origin',(0.692820323027551,0.,0.));
#7930=CARTESIAN_POINT('',(0.692820323027551,0.,0.));
#7931=CARTESIAN_POINT('Origin',(0.346410161513776,0.,0.6));
#7932=CARTESIAN_POINT('Origin',(0.46,0.7,0.));
#7933=CARTESIAN_POINT('',(-0.46,0.7,-5.63337527607782E-17));
#7934=CARTESIAN_POINT('Origin',(0.,0.7,0.));
#7935=CARTESIAN_POINT('Origin',(0.,1.2,0.));
#7936=CARTESIAN_POINT('',(-0.46,1.7,-5.63337527607782E-17));
#7937=CARTESIAN_POINT('',(-0.46,1.2,-5.63337527607782E-17));
#7938=CARTESIAN_POINT('Origin',(0.,1.7,0.));
#7939=CARTESIAN_POINT('Origin',(0.525,1.7,0.));
#7940=CARTESIAN_POINT('',(-0.525,1.7,-6.4293956955236E-17));
#7941=CARTESIAN_POINT('Origin',(0.,1.7,0.));
#7942=CARTESIAN_POINT('Origin',(0.,1.1,0.));
#7943=CARTESIAN_POINT('',(-0.525,1.1,-6.4293956955236E-17));
#7944=CARTESIAN_POINT('Origin',(0.,-0.325,0.));
#7945=CARTESIAN_POINT('',(-0.515,-0.65,-6.30693101560887E-17));
#7946=CARTESIAN_POINT('Origin',(0.,-0.65,0.));
#7947=CARTESIAN_POINT('',(-0.515,-0.325,-6.30693101560887E-17));
#7948=CARTESIAN_POINT('Origin',(0.2,-0.65,0.));
#7949=CARTESIAN_POINT('',(-0.2,-0.65,-2.44929359829471E-17));
#7950=CARTESIAN_POINT('Origin',(0.,-0.65,0.));
#7951=CARTESIAN_POINT('Origin',(0.,0.0249999999999999,0.));
#7952=CARTESIAN_POINT('',(-0.2,0.0249999999999999,-2.44929359829471E-17));
#8236=UNCERTAINTY_MEASURE_WITH_UNIT(LENGTH_MEASURE(0.001),#8267,
'DISTANCE_ACCURACY_VALUE',
'Maximum model space distance between geometric entities at asserted c
onnectivities');
#8241=UNCERTAINTY_MEASURE_WITH_UNIT(LENGTH_MEASURE(0.001),#8267,
'DISTANCE_ACCURACY_VALUE',
'Maximum model space distance between geometric entities at asserted c
onnectivities');
#8261=(
GEOMETRIC_REPRESENTATION_CONTEXT(3)
GLOBAL_UNCERTAINTY_ASSIGNED_CONTEXT((#8236))
GLOBAL_UNIT_ASSIGNED_CONTEXT((#8267,#8269,#8270))
REPRESENTATION_CONTEXT('','3D')
);
#8266=(
GEOMETRIC_REPRESENTATION_CONTEXT(3)
GLOBAL_UNCERTAINTY_ASSIGNED_CONTEXT((#8241))
GLOBAL_UNIT_ASSIGNED_CONTEXT((#8267,#8269,#8270))
REPRESENTATION_CONTEXT('','3D')
);
#8267=(
LENGTH_UNIT()
NAMED_UNIT(*)
SI_UNIT(.CENTI.,.METRE.)
);
#8269=(
NAMED_UNIT(*)
PLANE_ANGLE_UNIT()
SI_UNIT($,.RADIAN.)
);
#8270=(
NAMED_UNIT(*)
SI_UNIT($,.STERADIAN.)
SOLID_ANGLE_UNIT()
);
#8290=SHAPE_DEFINITION_REPRESENTATION(#8314,#8377);
#8314=PRODUCT_DEFINITION_SHAPE('',$,#8402);
#8377=SHAPE_REPRESENTATION('',(#5228),#8261);
#8382=PRODUCT_DEFINITION_CONTEXT('part definition',#8456,'design');
#8402=PRODUCT_DEFINITION('Body','Body',#8426,#8382);
#8426=PRODUCT_DEFINITION_FORMATION('',$,#8477);
#8456=APPLICATION_CONTEXT(
'Core Data for Automotive Mechanical Design Process');
#8457=PRODUCT_CONTEXT('part definition',#8456,'mechanical');
#8477=PRODUCT('Body','Body','Body',(#8457));
#8510=COLOUR_RGB('Dark Blue',0.08,0.2,0.34);
#8511=FILL_AREA_STYLE_COLOUR('',#8510);
#8512=FILL_AREA_STYLE('',(#8511));
#8513=SURFACE_STYLE_FILL_AREA(#8512);
#8514=SURFACE_SIDE_STYLE('',(#8513));
#8515=SURFACE_STYLE_USAGE(.BOTH.,#8514);
#8516=PRESENTATION_STYLE_ASSIGNMENT((#8515));
ENDSEC;
END-ISO-10303-21;
